ISO-10303-21;
HEADER;
/* Generated by software containing ST-Developer
 * from STEP Tools, Inc. (www.steptools.com) 
 */

FILE_DESCRIPTION(
/* description */ (''),
/* implementation_level */ '2;1');

FILE_NAME(
/* name */ 'Screw_02.step',
/* time_stamp */ '2026-10-06T13:23:02-07:00',
/* author */ (''),
/* organization */ (''),
/* preprocessor_version */ 'ST-DEVELOPER v20.2',
/* originating_system */ 'Autodesk Translation Framework v15.15.0.0',
/* authorisation */ '');

FILE_SCHEMA (('AUTOMOTIVE_DESIGN { 1 0 10303 214 3 1 1 }'));
ENDSEC;

DATA;
#10=MECHANICAL_DESIGN_GEOMETRIC_PRESENTATION_REPRESENTATION('',(#72),#4994);
#52=SHAPE_REPRESENTATION_RELATIONSHIP('SRR','None',#5033,#62);
#62=ADVANCED_BREP_SHAPE_REPRESENTATION('',(#82),#4985);
#72=STYLED_ITEM('',(#5091),#82);
#82=MANIFOLD_SOLID_BREP('Body1',#2912);
#93=CYLINDRICAL_SURFACE('',#3069,1.9);
#94=CYLINDRICAL_SURFACE('',#3083,0.96675);
#125=FACE_BOUND('',#505,.T.);
#126=FACE_BOUND('',#522,.T.);
#181=PLANE('',#3068);
#182=PLANE('',#3071);
#183=PLANE('',#3072);
#184=PLANE('',#3073);
#185=PLANE('',#3074);
#186=PLANE('',#3075);
#187=PLANE('',#3076);
#188=PLANE('',#3077);
#189=PLANE('',#3078);
#190=PLANE('',#3079);
#191=PLANE('',#3080);
#192=PLANE('',#3081);
#193=PLANE('',#3082);
#194=PLANE('',#3085);
#195=PLANE('',#3086);
#300=TOROIDAL_SURFACE('',#3064,1.7,0.2);
#322=FACE_OUTER_BOUND('',#502,.T.);
#323=FACE_OUTER_BOUND('',#503,.T.);
#324=FACE_OUTER_BOUND('',#504,.T.);
#325=FACE_OUTER_BOUND('',#506,.T.);
#326=FACE_OUTER_BOUND('',#507,.T.);
#327=FACE_OUTER_BOUND('',#508,.T.);
#328=FACE_OUTER_BOUND('',#509,.T.);
#329=FACE_OUTER_BOUND('',#510,.T.);
#330=FACE_OUTER_BOUND('',#511,.T.);
#331=FACE_OUTER_BOUND('',#512,.T.);
#332=FACE_OUTER_BOUND('',#513,.T.);
#333=FACE_OUTER_BOUND('',#514,.T.);
#334=FACE_OUTER_BOUND('',#515,.T.);
#335=FACE_OUTER_BOUND('',#516,.T.);
#336=FACE_OUTER_BOUND('',#517,.T.);
#337=FACE_OUTER_BOUND('',#518,.T.);
#338=FACE_OUTER_BOUND('',#519,.T.);
#339=FACE_OUTER_BOUND('',#520,.T.);
#340=FACE_OUTER_BOUND('',#521,.T.);
#502=EDGE_LOOP('',(#2044,#2045,#2046,#2047));
#503=EDGE_LOOP('',(#2048,#2049,#2050,#2051));
#504=EDGE_LOOP('',(#2052));
#505=EDGE_LOOP('',(#2053,#2054,#2055,#2056,#2057,#2058));
#506=EDGE_LOOP('',(#2059,#2060,#2061,#2062));
#507=EDGE_LOOP('',(#2063,#2064,#2065));
#508=EDGE_LOOP('',(#2066,#2067,#2068));
#509=EDGE_LOOP('',(#2069,#2070,#2071));
#510=EDGE_LOOP('',(#2072,#2073,#2074));
#511=EDGE_LOOP('',(#2075,#2076,#2077));
#512=EDGE_LOOP('',(#2078,#2079,#2080));
#513=EDGE_LOOP('',(#2081,#2082,#2083,#2084));
#514=EDGE_LOOP('',(#2085,#2086,#2087,#2088));
#515=EDGE_LOOP('',(#2089,#2090,#2091,#2092));
#516=EDGE_LOOP('',(#2093,#2094,#2095,#2096));
#517=EDGE_LOOP('',(#2097,#2098,#2099,#2100));
#518=EDGE_LOOP('',(#2101,#2102,#2103,#2104));
#519=EDGE_LOOP('',(#2105,#2106,#2107,#2108));
#520=EDGE_LOOP('',(#2109));
#521=EDGE_LOOP('',(#2110));
#522=EDGE_LOOP('',(#2111));
#729=LINE('',#4244,#1022);
#730=LINE('',#4255,#1023);
#731=LINE('',#4257,#1024);
#732=LINE('',#4259,#1025);
#733=LINE('',#4261,#1026);
#734=LINE('',#4263,#1027);
#735=LINE('',#4264,#1028);
#736=LINE('',#4268,#1029);
#737=LINE('',#4272,#1030);
#738=LINE('',#4274,#1031);
#739=LINE('',#4275,#1032);
#740=LINE('',#4278,#1033);
#741=LINE('',#4279,#1034);
#742=LINE('',#4282,#1035);
#743=LINE('',#4283,#1036);
#744=LINE('',#4286,#1037);
#745=LINE('',#4287,#1038);
#746=LINE('',#4290,#1039);
#747=LINE('',#4291,#1040);
#748=LINE('',#4293,#1041);
#749=LINE('',#4295,#1042);
#750=LINE('',#4296,#1043);
#751=LINE('',#4298,#1044);
#752=LINE('',#4300,#1045);
#753=LINE('',#4302,#1046);
#754=LINE('',#4304,#1047);
#755=LINE('',#4308,#1048);
#1022=VECTOR('',#3401,0.887310000000001);
#1023=VECTOR('',#3414,10.);
#1024=VECTOR('',#3415,10.);
#1025=VECTOR('',#3416,10.);
#1026=VECTOR('',#3417,10.);
#1027=VECTOR('',#3418,10.);
#1028=VECTOR('',#3419,10.);
#1029=VECTOR('',#3424,1.9);
#1030=VECTOR('',#3427,9.99999999999999);
#1031=VECTOR('',#3428,10.);
#1032=VECTOR('',#3429,10.);
#1033=VECTOR('',#3432,10.);
#1034=VECTOR('',#3433,10.);
#1035=VECTOR('',#3436,10.);
#1036=VECTOR('',#3437,9.99999999999999);
#1037=VECTOR('',#3440,10.);
#1038=VECTOR('',#3441,10.);
#1039=VECTOR('',#3444,10.);
#1040=VECTOR('',#3445,10.);
#1041=VECTOR('',#3448,10.);
#1042=VECTOR('',#3451,10.);
#1043=VECTOR('',#3452,10.);
#1044=VECTOR('',#3455,10.);
#1045=VECTOR('',#3458,10.);
#1046=VECTOR('',#3461,10.);
#1047=VECTOR('',#3464,10.);
#1048=VECTOR('',#3469,0.96675);
#1295=CIRCLE('',#3062,0.96675);
#1296=CIRCLE('',#3063,0.754619999999998);
#1297=CIRCLE('',#3065,1.9);
#1298=CIRCLE('',#3066,0.2);
#1299=CIRCLE('',#3067,1.7);
#1300=CIRCLE('',#3070,1.9);
#1301=CIRCLE('',#3084,0.96675);
#1388=VERTEX_POINT('',#4241);
#1389=VERTEX_POINT('',#4243);
#1390=VERTEX_POINT('',#4247);
#1391=VERTEX_POINT('',#4249);
#1392=VERTEX_POINT('',#4253);
#1393=VERTEX_POINT('',#4254);
#1394=VERTEX_POINT('',#4256);
#1395=VERTEX_POINT('',#4258);
#1396=VERTEX_POINT('',#4260);
#1397=VERTEX_POINT('',#4262);
#1398=VERTEX_POINT('',#4266);
#1399=VERTEX_POINT('',#4270);
#1400=VERTEX_POINT('',#4271);
#1401=VERTEX_POINT('',#4273);
#1402=VERTEX_POINT('',#4277);
#1403=VERTEX_POINT('',#4281);
#1404=VERTEX_POINT('',#4285);
#1405=VERTEX_POINT('',#4289);
#1406=VERTEX_POINT('',#4307);
#1636=EDGE_CURVE('',#1388,#1388,#1295,.T.);
#1637=EDGE_CURVE('',#1388,#1389,#729,.T.);
#1638=EDGE_CURVE('',#1389,#1389,#1296,.T.);
#1639=EDGE_CURVE('',#1390,#1390,#1297,.T.);
#1640=EDGE_CURVE('',#1390,#1391,#1298,.T.);
#1641=EDGE_CURVE('',#1391,#1391,#1299,.T.);
#1642=EDGE_CURVE('',#1392,#1393,#730,.T.);
#1643=EDGE_CURVE('',#1393,#1394,#731,.T.);
#1644=EDGE_CURVE('',#1394,#1395,#732,.T.);
#1645=EDGE_CURVE('',#1395,#1396,#733,.T.);
#1646=EDGE_CURVE('',#1396,#1397,#734,.T.);
#1647=EDGE_CURVE('',#1397,#1392,#735,.T.);
#1648=EDGE_CURVE('',#1398,#1398,#1300,.T.);
#1649=EDGE_CURVE('',#1398,#1390,#736,.T.);
#1650=EDGE_CURVE('',#1399,#1400,#737,.T.);
#1651=EDGE_CURVE('',#1401,#1399,#738,.T.);
#1652=EDGE_CURVE('',#1401,#1400,#739,.T.);
#1653=EDGE_CURVE('',#1402,#1401,#740,.T.);
#1654=EDGE_CURVE('',#1402,#1400,#741,.T.);
#1655=EDGE_CURVE('',#1403,#1402,#742,.T.);
#1656=EDGE_CURVE('',#1403,#1400,#743,.T.);
#1657=EDGE_CURVE('',#1404,#1403,#744,.T.);
#1658=EDGE_CURVE('',#1404,#1400,#745,.T.);
#1659=EDGE_CURVE('',#1405,#1404,#746,.T.);
#1660=EDGE_CURVE('',#1405,#1400,#747,.T.);
#1661=EDGE_CURVE('',#1399,#1405,#748,.T.);
#1662=EDGE_CURVE('',#1392,#1401,#749,.T.);
#1663=EDGE_CURVE('',#1393,#1399,#750,.T.);
#1664=EDGE_CURVE('',#1397,#1402,#751,.T.);
#1665=EDGE_CURVE('',#1396,#1403,#752,.T.);
#1666=EDGE_CURVE('',#1395,#1404,#753,.T.);
#1667=EDGE_CURVE('',#1394,#1405,#754,.T.);
#1668=EDGE_CURVE('',#1388,#1406,#755,.T.);
#1669=EDGE_CURVE('',#1406,#1406,#1301,.F.);
#2044=ORIENTED_EDGE('',*,*,#1636,.F.);
#2045=ORIENTED_EDGE('',*,*,#1637,.T.);
#2046=ORIENTED_EDGE('',*,*,#1638,.F.);
#2047=ORIENTED_EDGE('',*,*,#1637,.F.);
#2048=ORIENTED_EDGE('',*,*,#1639,.T.);
#2049=ORIENTED_EDGE('',*,*,#1640,.T.);
#2050=ORIENTED_EDGE('',*,*,#1641,.T.);
#2051=ORIENTED_EDGE('',*,*,#1640,.F.);
#2052=ORIENTED_EDGE('',*,*,#1641,.F.);
#2053=ORIENTED_EDGE('',*,*,#1642,.T.);
#2054=ORIENTED_EDGE('',*,*,#1643,.T.);
#2055=ORIENTED_EDGE('',*,*,#1644,.T.);
#2056=ORIENTED_EDGE('',*,*,#1645,.T.);
#2057=ORIENTED_EDGE('',*,*,#1646,.T.);
#2058=ORIENTED_EDGE('',*,*,#1647,.T.);
#2059=ORIENTED_EDGE('',*,*,#1648,.F.);
#2060=ORIENTED_EDGE('',*,*,#1649,.T.);
#2061=ORIENTED_EDGE('',*,*,#1639,.F.);
#2062=ORIENTED_EDGE('',*,*,#1649,.F.);
#2063=ORIENTED_EDGE('',*,*,#1650,.F.);
#2064=ORIENTED_EDGE('',*,*,#1651,.F.);
#2065=ORIENTED_EDGE('',*,*,#1652,.T.);
#2066=ORIENTED_EDGE('',*,*,#1652,.F.);
#2067=ORIENTED_EDGE('',*,*,#1653,.F.);
#2068=ORIENTED_EDGE('',*,*,#1654,.T.);
#2069=ORIENTED_EDGE('',*,*,#1654,.F.);
#2070=ORIENTED_EDGE('',*,*,#1655,.F.);
#2071=ORIENTED_EDGE('',*,*,#1656,.T.);
#2072=ORIENTED_EDGE('',*,*,#1656,.F.);
#2073=ORIENTED_EDGE('',*,*,#1657,.F.);
#2074=ORIENTED_EDGE('',*,*,#1658,.T.);
#2075=ORIENTED_EDGE('',*,*,#1658,.F.);
#2076=ORIENTED_EDGE('',*,*,#1659,.F.);
#2077=ORIENTED_EDGE('',*,*,#1660,.T.);
#2078=ORIENTED_EDGE('',*,*,#1660,.F.);
#2079=ORIENTED_EDGE('',*,*,#1661,.F.);
#2080=ORIENTED_EDGE('',*,*,#1650,.T.);
#2081=ORIENTED_EDGE('',*,*,#1642,.F.);
#2082=ORIENTED_EDGE('',*,*,#1662,.T.);
#2083=ORIENTED_EDGE('',*,*,#1651,.T.);
#2084=ORIENTED_EDGE('',*,*,#1663,.F.);
#2085=ORIENTED_EDGE('',*,*,#1647,.F.);
#2086=ORIENTED_EDGE('',*,*,#1664,.T.);
#2087=ORIENTED_EDGE('',*,*,#1653,.T.);
#2088=ORIENTED_EDGE('',*,*,#1662,.F.);
#2089=ORIENTED_EDGE('',*,*,#1646,.F.);
#2090=ORIENTED_EDGE('',*,*,#1665,.T.);
#2091=ORIENTED_EDGE('',*,*,#1655,.T.);
#2092=ORIENTED_EDGE('',*,*,#1664,.F.);
#2093=ORIENTED_EDGE('',*,*,#1645,.F.);
#2094=ORIENTED_EDGE('',*,*,#1666,.T.);
#2095=ORIENTED_EDGE('',*,*,#1657,.T.);
#2096=ORIENTED_EDGE('',*,*,#1665,.F.);
#2097=ORIENTED_EDGE('',*,*,#1644,.F.);
#2098=ORIENTED_EDGE('',*,*,#1667,.T.);
#2099=ORIENTED_EDGE('',*,*,#1659,.T.);
#2100=ORIENTED_EDGE('',*,*,#1666,.F.);
#2101=ORIENTED_EDGE('',*,*,#1643,.F.);
#2102=ORIENTED_EDGE('',*,*,#1663,.T.);
#2103=ORIENTED_EDGE('',*,*,#1661,.T.);
#2104=ORIENTED_EDGE('',*,*,#1667,.F.);
#2105=ORIENTED_EDGE('',*,*,#1636,.T.);
#2106=ORIENTED_EDGE('',*,*,#1668,.T.);
#2107=ORIENTED_EDGE('',*,*,#1669,.T.);
#2108=ORIENTED_EDGE('',*,*,#1668,.F.);
#2109=ORIENTED_EDGE('',*,*,#1638,.T.);
#2110=ORIENTED_EDGE('',*,*,#1648,.T.);
#2111=ORIENTED_EDGE('',*,*,#1669,.F.);
#2725=CONICAL_SURFACE('',#3061,0.887310000000001,0.824535502685815);
#2752=ADVANCED_FACE('',(#322),#2725,.T.);
#2753=ADVANCED_FACE('',(#323),#300,.T.);
#2754=ADVANCED_FACE('',(#324,#125),#181,.T.);
#2755=ADVANCED_FACE('',(#325),#93,.T.);
#2756=ADVANCED_FACE('',(#326),#182,.F.);
#2757=ADVANCED_FACE('',(#327),#183,.F.);
#2758=ADVANCED_FACE('',(#328),#184,.F.);
#2759=ADVANCED_FACE('',(#329),#185,.F.);
#2760=ADVANCED_FACE('',(#330),#186,.F.);
#2761=ADVANCED_FACE('',(#331),#187,.F.);
#2762=ADVANCED_FACE('',(#332),#188,.F.);
#2763=ADVANCED_FACE('',(#333),#189,.F.);
#2764=ADVANCED_FACE('',(#334),#190,.F.);
#2765=ADVANCED_FACE('',(#335),#191,.F.);
#2766=ADVANCED_FACE('',(#336),#192,.F.);
#2767=ADVANCED_FACE('',(#337),#193,.F.);
#2768=ADVANCED_FACE('',(#338),#94,.T.);
#2769=ADVANCED_FACE('',(#339),#194,.T.);
#2770=ADVANCED_FACE('',(#340,#126),#195,.T.);
#2912=CLOSED_SHELL('',(#2752,#2753,#2754,#2755,#2756,#2757,#2758,#2759,
#2760,#2761,#2762,#2763,#2764,#2765,#2766,#2767,#2768,#2769,#2770));
#3060=AXIS2_PLACEMENT_3D('',#4239,#3395,#3396);
#3061=AXIS2_PLACEMENT_3D('',#4240,#3397,#3398);
#3062=AXIS2_PLACEMENT_3D('',#4242,#3399,#3400);
#3063=AXIS2_PLACEMENT_3D('',#4245,#3402,#3403);
#3064=AXIS2_PLACEMENT_3D('',#4246,#3404,#3405);
#3065=AXIS2_PLACEMENT_3D('',#4248,#3406,#3407);
#3066=AXIS2_PLACEMENT_3D('',#4250,#3408,#3409);
#3067=AXIS2_PLACEMENT_3D('',#4251,#3410,#3411);
#3068=AXIS2_PLACEMENT_3D('',#4252,#3412,#3413);
#3069=AXIS2_PLACEMENT_3D('',#4265,#3420,#3421);
#3070=AXIS2_PLACEMENT_3D('',#4267,#3422,#3423);
#3071=AXIS2_PLACEMENT_3D('',#4269,#3425,#3426);
#3072=AXIS2_PLACEMENT_3D('',#4276,#3430,#3431);
#3073=AXIS2_PLACEMENT_3D('',#4280,#3434,#3435);
#3074=AXIS2_PLACEMENT_3D('',#4284,#3438,#3439);
#3075=AXIS2_PLACEMENT_3D('',#4288,#3442,#3443);
#3076=AXIS2_PLACEMENT_3D('',#4292,#3446,#3447);
#3077=AXIS2_PLACEMENT_3D('',#4294,#3449,#3450);
#3078=AXIS2_PLACEMENT_3D('',#4297,#3453,#3454);
#3079=AXIS2_PLACEMENT_3D('',#4299,#3456,#3457);
#3080=AXIS2_PLACEMENT_3D('',#4301,#3459,#3460);
#3081=AXIS2_PLACEMENT_3D('',#4303,#3462,#3463);
#3082=AXIS2_PLACEMENT_3D('',#4305,#3465,#3466);
#3083=AXIS2_PLACEMENT_3D('',#4306,#3467,#3468);
#3084=AXIS2_PLACEMENT_3D('',#4309,#3470,#3471);
#3085=AXIS2_PLACEMENT_3D('',#4310,#3472,#3473);
#3086=AXIS2_PLACEMENT_3D('',#4311,#3474,#3475);
#3395=DIRECTION('axis',(0.,0.,1.));
#3396=DIRECTION('refdir',(1.,0.,0.));
#3397=DIRECTION('center_axis',(0.,0.,1.));
#3398=DIRECTION('ref_axis',(-1.,0.,0.));
#3399=DIRECTION('center_axis',(-1.06387651071382E-15,0.,1.));
#3400=DIRECTION('ref_axis',(-1.,0.,-1.06387651071382E-15));
#3401=DIRECTION('',(-0.73423251512767,-8.99175499481012E-17,-0.678898087881602));
#3402=DIRECTION('center_axis',(1.06387651071382E-15,0.,-1.));
#3403=DIRECTION('ref_axis',(-1.,0.,-1.06387651071382E-15));
#3404=DIRECTION('center_axis',(1.06387651071382E-15,0.,-1.));
#3405=DIRECTION('ref_axis',(-1.,0.,-1.05179023385541E-15));
#3406=DIRECTION('center_axis',(-1.06387651071382E-15,0.,1.));
#3407=DIRECTION('ref_axis',(1.,0.,1.06387651071382E-15));
#3408=DIRECTION('center_axis',(-1.22464679914735E-16,-1.,-1.30287296353373E-31));
#3409=DIRECTION('ref_axis',(1.,-1.22464679914735E-16,1.02257383847054E-15));
#3410=DIRECTION('center_axis',(1.06387651071382E-15,0.,-1.));
#3411=DIRECTION('ref_axis',(1.,0.,1.06387651071382E-15));
#3412=DIRECTION('center_axis',(-1.06387651071382E-15,0.,1.));
#3413=DIRECTION('ref_axis',(1.,0.,1.06387651071382E-15));
#3414=DIRECTION('',(-0.866025403784439,-0.5,-9.21344084767719E-16));
#3415=DIRECTION('',(-0.866025403784439,0.5,-9.21344084767719E-16));
#3416=DIRECTION('',(6.40987562127854E-16,1.,6.81931611007542E-31));
#3417=DIRECTION('',(0.866025403784439,0.5,9.21344084767719E-16));
#3418=DIRECTION('',(0.866025403784439,-0.5,9.21344084767719E-16));
#3419=DIRECTION('',(-1.60246890531964E-16,-1.,-1.70482902751885E-31));
#3420=DIRECTION('center_axis',(1.06387651071382E-15,0.,-1.));
#3421=DIRECTION('ref_axis',(-1.,0.,-1.06387651071382E-15));
#3422=DIRECTION('center_axis',(1.06387651071382E-15,0.,-1.));
#3423=DIRECTION('ref_axis',(1.,0.,1.06387651071382E-15));
#3424=DIRECTION('',(-1.06387651071382E-15,0.,1.));
#3425=DIRECTION('center_axis',(0.0435778713738291,-0.0754790873051733,-0.996194698091746));
#3426=DIRECTION('ref_axis',(-0.866025403784439,-0.5,-3.35810244624808E-17));
#3427=DIRECTION('',(0.,0.997141949694316,-0.0755508581011305));
#3428=DIRECTION('',(-0.866025403784439,-0.5,0.));
#3429=DIRECTION('',(-0.863550259614423,0.498570974847158,-0.0755508581011305));
#3430=DIRECTION('center_axis',(0.0871557427476581,-1.3966436767316E-17,
-0.996194698091746));
#3431=DIRECTION('ref_axis',(-1.60246890531964E-16,-1.,1.77292017095641E-32));
#3432=DIRECTION('',(-1.60246890531964E-16,-1.,0.));
#3433=DIRECTION('',(-0.863550259614423,-0.498570974847158,-0.0755508581011305));
#3434=DIRECTION('center_axis',(0.0435778713738291,0.0754790873051733,-0.996194698091746));
#3435=DIRECTION('ref_axis',(0.866025403784439,-0.5,3.35810244624808E-17));
#3436=DIRECTION('',(0.866025403784439,-0.5,0.));
#3437=DIRECTION('',(-1.59381164582915E-16,-0.997141949694316,-0.0755508581011305));
#3438=DIRECTION('center_axis',(-0.0435778713738291,0.0754790873051733,-0.996194698091746));
#3439=DIRECTION('ref_axis',(0.866025403784439,0.5,-3.35810244624808E-17));
#3440=DIRECTION('',(0.866025403784439,0.5,0.));
#3441=DIRECTION('',(0.863550259614423,-0.498570974847159,-0.0755508581011305));
#3442=DIRECTION('center_axis',(-0.0871557427476581,5.58657470692638E-17,
-0.996194698091746));
#3443=DIRECTION('ref_axis',(6.40987562127854E-16,1.,4.7015367027096E-32));
#3444=DIRECTION('',(6.40987562127854E-16,1.,0.));
#3445=DIRECTION('',(0.863550259614423,0.498570974847158,-0.0755508581011305));
#3446=DIRECTION('center_axis',(-0.0435778713738291,-0.0754790873051733,
-0.996194698091746));
#3447=DIRECTION('ref_axis',(-0.866025403784439,0.5,3.35810244624808E-17));
#3448=DIRECTION('',(-0.866025403784439,0.5,0.));
#3449=DIRECTION('center_axis',(0.5,-0.866025403784439,0.));
#3450=DIRECTION('ref_axis',(-0.866025403784439,-0.5,0.));
#3451=DIRECTION('',(0.,0.,-1.));
#3452=DIRECTION('',(0.,0.,-1.));
#3453=DIRECTION('center_axis',(1.,-1.60246890531964E-16,0.));
#3454=DIRECTION('ref_axis',(-1.60246890531964E-16,-1.,0.));
#3455=DIRECTION('',(0.,0.,-1.));
#3456=DIRECTION('center_axis',(0.5,0.866025403784439,0.));
#3457=DIRECTION('ref_axis',(0.866025403784439,-0.5,0.));
#3458=DIRECTION('',(0.,0.,-1.));
#3459=DIRECTION('center_axis',(-0.5,0.866025403784439,0.));
#3460=DIRECTION('ref_axis',(0.866025403784439,0.5,0.));
#3461=DIRECTION('',(0.,0.,-1.));
#3462=DIRECTION('center_axis',(-1.,6.40987562127854E-16,0.));
#3463=DIRECTION('ref_axis',(6.40987562127854E-16,1.,0.));
#3464=DIRECTION('',(0.,0.,-1.));
#3465=DIRECTION('center_axis',(-0.5,-0.866025403784439,0.));
#3466=DIRECTION('ref_axis',(-0.866025403784439,0.5,0.));
#3467=DIRECTION('center_axis',(1.06387651071382E-15,0.,-1.));
#3468=DIRECTION('ref_axis',(-1.,0.,-1.06387651071382E-15));
#3469=DIRECTION('',(-1.06387651071382E-15,0.,1.));
#3470=DIRECTION('center_axis',(-1.06387651071382E-15,0.,1.));
#3471=DIRECTION('ref_axis',(-1.,0.,-1.06387651071382E-15));
#3472=DIRECTION('center_axis',(1.06387651071382E-15,0.,-1.));
#3473=DIRECTION('ref_axis',(-1.,0.,-1.06387651071382E-15));
#3474=DIRECTION('center_axis',(1.06387651071382E-15,0.,-1.));
#3475=DIRECTION('ref_axis',(-1.,0.,-1.06387651071382E-15));
#4239=CARTESIAN_POINT('',(0.,0.,0.));
#4240=CARTESIAN_POINT('Origin',(0.,0.,-4.87731));
#4241=CARTESIAN_POINT('',(0.966750000000005,1.1839272930757E-16,-4.80385688672847));
#4242=CARTESIAN_POINT('Origin',(5.11071050262126E-15,0.,-4.80385688672847));
#4243=CARTESIAN_POINT('',(0.754619999999998,-9.24142967572573E-17,-5.));
#4244=CARTESIAN_POINT('',(0.887310000000001,1.08664135135144E-16,-4.87731));
#4245=CARTESIAN_POINT('Origin',(0.,0.,-5.));
#4246=CARTESIAN_POINT('Origin',(-1.91497771928438E-15,0.,1.79999999999952));
#4247=CARTESIAN_POINT('',(1.89999999999999,-2.32682891837997E-16,1.79999999999953));
#4248=CARTESIAN_POINT('Origin',(-1.91497771928438E-15,0.,1.79999999999952));
#4249=CARTESIAN_POINT('',(1.69999999999999,-2.0818995585505E-16,1.99999999999953));
#4250=CARTESIAN_POINT('Origin',(1.7,-2.0818995585505E-16,1.79999999999952));
#4251=CARTESIAN_POINT('Origin',(-2.12775302142714E-15,0.,1.99999999999952));
#4252=CARTESIAN_POINT('Origin',(-1.9,0.,1.99999999999952));
#4253=CARTESIAN_POINT('',(0.75,-0.433012701892219,2.));
#4254=CARTESIAN_POINT('',(1.38777878078145E-16,-0.866025403784439,2.));
#4255=CARTESIAN_POINT('',(-0.149999999999999,-0.952627944162883,1.99999999999952));
#4256=CARTESIAN_POINT('',(-0.750000000000001,-0.433012701892219,2.));
#4257=CARTESIAN_POINT('',(-0.899999999999999,-0.346410161513776,1.99999999999952));
#4258=CARTESIAN_POINT('',(-0.75,0.43301270189222,2.));
#4259=CARTESIAN_POINT('',(-0.75,-0.21650635094611,1.99999999999952));
#4260=CARTESIAN_POINT('',(1.73472347597681E-17,0.866025403784439,2.));
#4261=CARTESIAN_POINT('',(-1.275,0.129903810567666,1.99999999999952));
#4262=CARTESIAN_POINT('',(0.75,0.433012701892219,2.));
#4263=CARTESIAN_POINT('',(-0.524999999999999,1.16913429510899,1.99999999999952));
#4264=CARTESIAN_POINT('',(0.75,0.216506350946109,1.99999999999952));
#4265=CARTESIAN_POINT('Origin',(-1.06387651071333E-15,0.,0.999999999999538));
#4266=CARTESIAN_POINT('',(1.9,-2.32682891837997E-16,-4.47419878923938E-13));
#4267=CARTESIAN_POINT('Origin',(4.74691816123085E-28,0.,-4.48558184615945E-13));
#4268=CARTESIAN_POINT('',(1.9,-2.32682891837997E-16,0.99999999999954));
#4269=CARTESIAN_POINT('Origin',(1.38777878078145E-16,-0.866025403784439,
1.));
#4270=CARTESIAN_POINT('',(1.38777878078145E-16,-0.866025403784439,1.));
#4271=CARTESIAN_POINT('',(0.,2.77555756156289E-16,0.934383502355557));
#4272=CARTESIAN_POINT('',(0.,-0.650754856401699,0.983689509218169));
#4273=CARTESIAN_POINT('',(0.75,-0.433012701892219,1.));
#4274=CARTESIAN_POINT('',(8.5846548499269E-17,-0.866025403784439,1.));
#4275=CARTESIAN_POINT('',(0.563570237279966,-0.325377428200849,0.983689509218169));
#4276=CARTESIAN_POINT('Origin',(0.75,-0.433012701892219,1.));
#4277=CARTESIAN_POINT('',(0.75,0.433012701892219,1.));
#4278=CARTESIAN_POINT('',(0.75,-0.433012701892219,1.));
#4279=CARTESIAN_POINT('',(0.563570237279966,0.32537742820085,0.983689509218169));
#4280=CARTESIAN_POINT('Origin',(0.75,0.433012701892219,1.));
#4281=CARTESIAN_POINT('',(0.,0.866025403784439,1.));
#4282=CARTESIAN_POINT('',(0.75,0.433012701892219,1.));
#4283=CARTESIAN_POINT('',(0.,0.650754856401699,0.983689509218169));
#4284=CARTESIAN_POINT('Origin',(0.,0.866025403784439,1.));
#4285=CARTESIAN_POINT('',(-0.75,0.43301270189222,1.));
#4286=CARTESIAN_POINT('',(1.73472347597681E-17,0.866025403784439,1.));
#4287=CARTESIAN_POINT('',(-0.563570237279966,0.325377428200849,0.983689509218169));
#4288=CARTESIAN_POINT('Origin',(-0.75,0.43301270189222,1.));
#4289=CARTESIAN_POINT('',(-0.750000000000001,-0.433012701892219,1.));
#4290=CARTESIAN_POINT('',(-0.75,0.43301270189222,1.));
#4291=CARTESIAN_POINT('',(-0.563570237279966,-0.325377428200849,0.983689509218169));
#4292=CARTESIAN_POINT('Origin',(-0.750000000000001,-0.433012701892219,1.));
#4293=CARTESIAN_POINT('',(-0.750000000000001,-0.433012701892219,1.));
#4294=CARTESIAN_POINT('Origin',(0.75,-0.433012701892219,2.));
#4295=CARTESIAN_POINT('',(0.75,-0.433012701892219,2.));
#4296=CARTESIAN_POINT('',(1.38777878078145E-16,-0.866025403784439,2.));
#4297=CARTESIAN_POINT('Origin',(0.75,0.433012701892219,2.));
#4298=CARTESIAN_POINT('',(0.75,0.433012701892219,2.));
#4299=CARTESIAN_POINT('Origin',(0.,0.866025403784439,2.));
#4300=CARTESIAN_POINT('',(1.73472347597681E-17,0.866025403784439,2.));
#4301=CARTESIAN_POINT('Origin',(-0.75,0.43301270189222,2.));
#4302=CARTESIAN_POINT('',(-0.75,0.43301270189222,2.));
#4303=CARTESIAN_POINT('Origin',(-0.750000000000001,-0.433012701892219,2.));
#4304=CARTESIAN_POINT('',(-0.750000000000001,-0.433012701892219,2.));
#4305=CARTESIAN_POINT('Origin',(1.38777878078145E-16,-0.866025403784439,
2.));
#4306=CARTESIAN_POINT('Origin',(2.65969127678468E-15,0.,-2.50000000000012));
#4307=CARTESIAN_POINT('',(0.96675,1.1839272930757E-16,-2.35150733091162E-13));
#4308=CARTESIAN_POINT('',(0.966750000000003,-1.1839272930757E-16,-2.50000000000012));
#4309=CARTESIAN_POINT('Origin',(2.48491185144619E-28,0.,-2.35922392732846E-13));
#4310=CARTESIAN_POINT('Origin',(5.27355936696949E-15,0.,-5.));
#4311=CARTESIAN_POINT('Origin',(-0.999999999999996,0.,-2.37147131571737E-13));
#4973=UNCERTAINTY_MEASURE_WITH_UNIT(LENGTH_MEASURE(0.01),#4995,
'DISTANCE_ACCURACY_VALUE',
'Maximum model space distance between geometric entities at asserted c
onnectivities');
#4982=UNCERTAINTY_MEASURE_WITH_UNIT(LENGTH_MEASURE(0.01),#4995,
'DISTANCE_ACCURACY_VALUE',
'Maximum model space distance between geometric entities at asserted c
onnectivities');
#4985=(
GEOMETRIC_REPRESENTATION_CONTEXT(3)
GLOBAL_UNCERTAINTY_ASSIGNED_CONTEXT((#4973))
GLOBAL_UNIT_ASSIGNED_CONTEXT((#4995,#4997,#4998))
REPRESENTATION_CONTEXT('','3D')
);
#4994=(
GEOMETRIC_REPRESENTATION_CONTEXT(3)
GLOBAL_UNCERTAINTY_ASSIGNED_CONTEXT((#4982))
GLOBAL_UNIT_ASSIGNED_CONTEXT((#4995,#4997,#4998))
REPRESENTATION_CONTEXT('','3D')
);
#4995=(
LENGTH_UNIT()
NAMED_UNIT(*)
SI_UNIT(.MILLI.,.METRE.)
);
#4997=(
NAMED_UNIT(*)
PLANE_ANGLE_UNIT()
SI_UNIT($,.RADIAN.)
);
#4998=(
NAMED_UNIT(*)
SI_UNIT($,.STERADIAN.)
SOLID_ANGLE_UNIT()
);
#5001=SHAPE_DEFINITION_REPRESENTATION(#5012,#5033);
#5012=PRODUCT_DEFINITION_SHAPE('',$,#5045);
#5033=SHAPE_REPRESENTATION('',(#3060),#4985);
#5042=PRODUCT_DEFINITION_CONTEXT('part definition',#5077,'design');
#5045=PRODUCT_DEFINITION(
'BSHCS ASME B18.3.1M - M2x0.4 x 5 Steel Grade 2 Plain_1','Screw_02',#5056,
#5042);
#5056=PRODUCT_DEFINITION_FORMATION('',$,#5081);
#5077=APPLICATION_CONTEXT(
'Core Data for Automotive Mechanical Design Process');
#5078=PRODUCT_CONTEXT('part definition',#5077,'mechanical');
#5081=PRODUCT('BSHCS ASME B18.3.1M - M2x0.4 x 5 Steel Grade 2 Plain_1',
'Screw_02',
'Broached Hexagon Socket Head Cap Screw ASME B18.3.1M - M2x0.4 x 5',(#5078));
#5091=PRESENTATION_STYLE_ASSIGNMENT((#5096));
#5096=SURFACE_STYLE_USAGE(.BOTH.,#5101);
#5101=SURFACE_SIDE_STYLE('',(#5106));
#5106=SURFACE_STYLE_FILL_AREA(#5111);
#5111=FILL_AREA_STYLE('Opaque(160,160,160)',(#5116));
#5116=FILL_AREA_STYLE_COLOUR('Opaque(160,160,160)',#5121);
#5121=COLOUR_RGB('Opaque(160,160,160)', 0.09019608, 0.27058824, 0.51372549);
ENDSEC;
END-ISO-10303-21;
